ISO-10303-21;
HEADER;
/* Generated by software containing ST-Developer
 * from STEP Tools, Inc. (www.steptools.com) 
 */

FILE_DESCRIPTION(
/* description */ ('Cam-driven reciprocating slide'),
/* implementation_level */ '2;1');

FILE_NAME(
/* name */ 'Bearing cap (3).step',
/* time_stamp */ '2026-10-28T03:25:20-07:00',
/* author */ (''),
/* organization */ (''),
/* preprocessor_version */ 'ST-DEVELOPER v20.2',
/* originating_system */ 'Autodesk Translation Framework v15.17.0.0',
/* authorisation */ '');

FILE_SCHEMA (('AUTOMOTIVE_DESIGN { 1 0 10303 214 3 1 1 }'));
ENDSEC;

DATA;
#10=MECHANICAL_DESIGN_GEOMETRIC_PRESENTATION_REPRESENTATION('',(#430),#13277);
#356=SHAPE_REPRESENTATION_RELATIONSHIP('SRR','None',#13449,#393);
#393=ADVANCED_BREP_SHAPE_REPRESENTATION('',(#474),#13244);
#430=STYLED_ITEM('',(#13720),#474);
#474=MANIFOLD_SOLID_BREP('Body1',#6406);
#581=FACE_BOUND('',#1453,.T.);
#582=FACE_BOUND('',#1457,.T.);
#583=FACE_BOUND('',#1458,.T.);
#584=FACE_BOUND('',#1459,.T.);
#585=FACE_BOUND('',#1460,.T.);
#586=FACE_BOUND('',#1461,.T.);
#587=FACE_BOUND('',#1463,.T.);
#588=FACE_BOUND('',#1464,.T.);
#589=FACE_BOUND('',#1465,.T.);
#590=FACE_BOUND('',#1466,.T.);
#591=FACE_BOUND('',#1467,.T.);
#733=PLANE('',#7054);
#734=PLANE('',#7061);
#735=PLANE('',#7062);
#994=FACE_OUTER_BOUND('',#1447,.T.);
#995=FACE_OUTER_BOUND('',#1448,.T.);
#996=FACE_OUTER_BOUND('',#1449,.T.);
#997=FACE_OUTER_BOUND('',#1450,.T.);
#998=FACE_OUTER_BOUND('',#1451,.T.);
#999=FACE_OUTER_BOUND('',#1452,.T.);
#1000=FACE_OUTER_BOUND('',#1454,.T.);
#1001=FACE_OUTER_BOUND('',#1455,.T.);
#1002=FACE_OUTER_BOUND('',#1456,.T.);
#1003=FACE_OUTER_BOUND('',#1462,.T.);
#1447=EDGE_LOOP('',(#4774,#4775,#4776,#4777));
#1448=EDGE_LOOP('',(#4778,#4779,#4780,#4781));
#1449=EDGE_LOOP('',(#4782,#4783,#4784,#4785));
#1450=EDGE_LOOP('',(#4786,#4787,#4788,#4789));
#1451=EDGE_LOOP('',(#4790,#4791,#4792,#4793));
#1452=EDGE_LOOP('',(#4794));
#1453=EDGE_LOOP('',(#4795));
#1454=EDGE_LOOP('',(#4796,#4797,#4798,#4799));
#1455=EDGE_LOOP('',(#4800,#4801,#4802,#4803));
#1456=EDGE_LOOP('',(#4804));
#1457=EDGE_LOOP('',(#4805));
#1458=EDGE_LOOP('',(#4806));
#1459=EDGE_LOOP('',(#4807));
#1460=EDGE_LOOP('',(#4808));
#1461=EDGE_LOOP('',(#4809));
#1462=EDGE_LOOP('',(#4810));
#1463=EDGE_LOOP('',(#4811));
#1464=EDGE_LOOP('',(#4812));
#1465=EDGE_LOOP('',(#4813));
#1466=EDGE_LOOP('',(#4814));
#1467=EDGE_LOOP('',(#4815));
#1970=LINE('',#10213,#2409);
#1971=LINE('',#10219,#2410);
#1972=LINE('',#10225,#2411);
#1973=LINE('',#10231,#2412);
#1974=LINE('',#10237,#2413);
#1975=LINE('',#10245,#2414);
#1976=LINE('',#10250,#2415);
#2409=VECTOR('',#8182,0.225);
#2410=VECTOR('',#8189,0.225);
#2411=VECTOR('',#8196,0.225);
#2412=VECTOR('',#8203,0.225);
#2413=VECTOR('',#8210,1.59);
#2414=VECTOR('',#8221,1.005);
#2415=VECTOR('',#8226,2.4);
#2793=CIRCLE('',#7040,0.225);
#2794=CIRCLE('',#7041,0.225);
#2795=CIRCLE('',#7043,0.225);
#2796=CIRCLE('',#7044,0.225);
#2797=CIRCLE('',#7046,0.225);
#2798=CIRCLE('',#7047,0.225);
#2799=CIRCLE('',#7049,0.225);
#2800=CIRCLE('',#7050,0.225);
#2801=CIRCLE('',#7052,1.59);
#2802=CIRCLE('',#7053,1.59);
#2803=CIRCLE('',#7055,1.005);
#2804=CIRCLE('',#7057,1.005);
#2805=CIRCLE('',#7059,2.4);
#2806=CIRCLE('',#7060,2.4);
#3181=VERTEX_POINT('',#10210);
#3182=VERTEX_POINT('',#10212);
#3183=VERTEX_POINT('',#10216);
#3184=VERTEX_POINT('',#10218);
#3185=VERTEX_POINT('',#10222);
#3186=VERTEX_POINT('',#10224);
#3187=VERTEX_POINT('',#10228);
#3188=VERTEX_POINT('',#10230);
#3189=VERTEX_POINT('',#10234);
#3190=VERTEX_POINT('',#10236);
#3191=VERTEX_POINT('',#10240);
#3192=VERTEX_POINT('',#10243);
#3193=VERTEX_POINT('',#10247);
#3194=VERTEX_POINT('',#10249);
#3777=EDGE_CURVE('',#3181,#3181,#2793,.T.);
#3778=EDGE_CURVE('',#3181,#3182,#1970,.T.);
#3779=EDGE_CURVE('',#3182,#3182,#2794,.T.);
#3780=EDGE_CURVE('',#3183,#3183,#2795,.T.);
#3781=EDGE_CURVE('',#3183,#3184,#1971,.T.);
#3782=EDGE_CURVE('',#3184,#3184,#2796,.T.);
#3783=EDGE_CURVE('',#3185,#3185,#2797,.T.);
#3784=EDGE_CURVE('',#3185,#3186,#1972,.T.);
#3785=EDGE_CURVE('',#3186,#3186,#2798,.T.);
#3786=EDGE_CURVE('',#3187,#3187,#2799,.T.);
#3787=EDGE_CURVE('',#3187,#3188,#1973,.T.);
#3788=EDGE_CURVE('',#3188,#3188,#2800,.T.);
#3789=EDGE_CURVE('',#3189,#3189,#2801,.T.);
#3790=EDGE_CURVE('',#3189,#3190,#1974,.T.);
#3791=EDGE_CURVE('',#3190,#3190,#2802,.T.);
#3792=EDGE_CURVE('',#3191,#3191,#2803,.T.);
#3793=EDGE_CURVE('',#3192,#3192,#2804,.T.);
#3794=EDGE_CURVE('',#3192,#3191,#1975,.T.);
#3795=EDGE_CURVE('',#3193,#3193,#2805,.T.);
#3796=EDGE_CURVE('',#3193,#3194,#1976,.T.);
#3797=EDGE_CURVE('',#3194,#3194,#2806,.T.);
#4774=ORIENTED_EDGE('',*,*,#3777,.F.);
#4775=ORIENTED_EDGE('',*,*,#3778,.T.);
#4776=ORIENTED_EDGE('',*,*,#3779,.F.);
#4777=ORIENTED_EDGE('',*,*,#3778,.F.);
#4778=ORIENTED_EDGE('',*,*,#3780,.F.);
#4779=ORIENTED_EDGE('',*,*,#3781,.T.);
#4780=ORIENTED_EDGE('',*,*,#3782,.F.);
#4781=ORIENTED_EDGE('',*,*,#3781,.F.);
#4782=ORIENTED_EDGE('',*,*,#3783,.F.);
#4783=ORIENTED_EDGE('',*,*,#3784,.T.);
#4784=ORIENTED_EDGE('',*,*,#3785,.F.);
#4785=ORIENTED_EDGE('',*,*,#3784,.F.);
#4786=ORIENTED_EDGE('',*,*,#3786,.F.);
#4787=ORIENTED_EDGE('',*,*,#3787,.T.);
#4788=ORIENTED_EDGE('',*,*,#3788,.F.);
#4789=ORIENTED_EDGE('',*,*,#3787,.F.);
#4790=ORIENTED_EDGE('',*,*,#3789,.F.);
#4791=ORIENTED_EDGE('',*,*,#3790,.T.);
#4792=ORIENTED_EDGE('',*,*,#3791,.T.);
#4793=ORIENTED_EDGE('',*,*,#3790,.F.);
#4794=ORIENTED_EDGE('',*,*,#3791,.F.);
#4795=ORIENTED_EDGE('',*,*,#3792,.F.);
#4796=ORIENTED_EDGE('',*,*,#3793,.F.);
#4797=ORIENTED_EDGE('',*,*,#3794,.T.);
#4798=ORIENTED_EDGE('',*,*,#3792,.T.);
#4799=ORIENTED_EDGE('',*,*,#3794,.F.);
#4800=ORIENTED_EDGE('',*,*,#3795,.F.);
#4801=ORIENTED_EDGE('',*,*,#3796,.T.);
#4802=ORIENTED_EDGE('',*,*,#3797,.T.);
#4803=ORIENTED_EDGE('',*,*,#3796,.F.);
#4804=ORIENTED_EDGE('',*,*,#3795,.T.);
#4805=ORIENTED_EDGE('',*,*,#3793,.T.);
#4806=ORIENTED_EDGE('',*,*,#3788,.T.);
#4807=ORIENTED_EDGE('',*,*,#3785,.T.);
#4808=ORIENTED_EDGE('',*,*,#3782,.T.);
#4809=ORIENTED_EDGE('',*,*,#3779,.T.);
#4810=ORIENTED_EDGE('',*,*,#3797,.F.);
#4811=ORIENTED_EDGE('',*,*,#3789,.T.);
#4812=ORIENTED_EDGE('',*,*,#3786,.T.);
#4813=ORIENTED_EDGE('',*,*,#3783,.T.);
#4814=ORIENTED_EDGE('',*,*,#3780,.T.);
#4815=ORIENTED_EDGE('',*,*,#3777,.T.);
#5933=CYLINDRICAL_SURFACE('',#7039,0.225);
#5934=CYLINDRICAL_SURFACE('',#7042,0.225);
#5935=CYLINDRICAL_SURFACE('',#7045,0.225);
#5936=CYLINDRICAL_SURFACE('',#7048,0.225);
#5937=CYLINDRICAL_SURFACE('',#7051,1.59);
#5938=CYLINDRICAL_SURFACE('',#7056,1.005);
#5939=CYLINDRICAL_SURFACE('',#7058,2.4);
#6112=ADVANCED_FACE('',(#994),#5933,.F.);
#6113=ADVANCED_FACE('',(#995),#5934,.F.);
#6114=ADVANCED_FACE('',(#996),#5935,.F.);
#6115=ADVANCED_FACE('',(#997),#5936,.F.);
#6116=ADVANCED_FACE('',(#998),#5937,.T.);
#6117=ADVANCED_FACE('',(#999,#581),#733,.F.);
#6118=ADVANCED_FACE('',(#1000),#5938,.F.);
#6119=ADVANCED_FACE('',(#1001),#5939,.T.);
#6120=ADVANCED_FACE('',(#1002,#582,#583,#584,#585,#586),#734,.T.);
#6121=ADVANCED_FACE('',(#1003,#587,#588,#589,#590,#591),#735,.F.);
#6406=CLOSED_SHELL('',(#6112,#6113,#6114,#6115,#6116,#6117,#6118,#6119,
#6120,#6121));
#7038=AXIS2_PLACEMENT_3D('',#10208,#8176,#8177);
#7039=AXIS2_PLACEMENT_3D('',#10209,#8178,#8179);
#7040=AXIS2_PLACEMENT_3D('',#10211,#8180,#8181);
#7041=AXIS2_PLACEMENT_3D('',#10214,#8183,#8184);
#7042=AXIS2_PLACEMENT_3D('',#10215,#8185,#8186);
#7043=AXIS2_PLACEMENT_3D('',#10217,#8187,#8188);
#7044=AXIS2_PLACEMENT_3D('',#10220,#8190,#8191);
#7045=AXIS2_PLACEMENT_3D('',#10221,#8192,#8193);
#7046=AXIS2_PLACEMENT_3D('',#10223,#8194,#8195);
#7047=AXIS2_PLACEMENT_3D('',#10226,#8197,#8198);
#7048=AXIS2_PLACEMENT_3D('',#10227,#8199,#8200);
#7049=AXIS2_PLACEMENT_3D('',#10229,#8201,#8202);
#7050=AXIS2_PLACEMENT_3D('',#10232,#8204,#8205);
#7051=AXIS2_PLACEMENT_3D('',#10233,#8206,#8207);
#7052=AXIS2_PLACEMENT_3D('',#10235,#8208,#8209);
#7053=AXIS2_PLACEMENT_3D('',#10238,#8211,#8212);
#7054=AXIS2_PLACEMENT_3D('',#10239,#8213,#8214);
#7055=AXIS2_PLACEMENT_3D('',#10241,#8215,#8216);
#7056=AXIS2_PLACEMENT_3D('',#10242,#8217,#8218);
#7057=AXIS2_PLACEMENT_3D('',#10244,#8219,#8220);
#7058=AXIS2_PLACEMENT_3D('',#10246,#8222,#8223);
#7059=AXIS2_PLACEMENT_3D('',#10248,#8224,#8225);
#7060=AXIS2_PLACEMENT_3D('',#10251,#8227,#8228);
#7061=AXIS2_PLACEMENT_3D('',#10252,#8229,#8230);
#7062=AXIS2_PLACEMENT_3D('',#10253,#8231,#8232);
#8176=DIRECTION('axis',(0.,0.,1.));
#8177=DIRECTION('refdir',(1.,0.,0.));
#8178=DIRECTION('center_axis',(0.,1.,0.));
#8179=DIRECTION('ref_axis',(1.,0.,0.));
#8180=DIRECTION('center_axis',(0.,1.,0.));
#8181=DIRECTION('ref_axis',(1.,0.,0.));
#8182=DIRECTION('',(0.,1.,0.));
#8183=DIRECTION('center_axis',(0.,-1.,0.));
#8184=DIRECTION('ref_axis',(1.,0.,0.));
#8185=DIRECTION('center_axis',(0.,1.,0.));
#8186=DIRECTION('ref_axis',(1.,0.,0.));
#8187=DIRECTION('center_axis',(0.,1.,0.));
#8188=DIRECTION('ref_axis',(1.,0.,0.));
#8189=DIRECTION('',(0.,1.,0.));
#8190=DIRECTION('center_axis',(0.,-1.,0.));
#8191=DIRECTION('ref_axis',(1.,0.,0.));
#8192=DIRECTION('center_axis',(0.,1.,0.));
#8193=DIRECTION('ref_axis',(1.,0.,0.));
#8194=DIRECTION('center_axis',(0.,1.,0.));
#8195=DIRECTION('ref_axis',(1.,0.,0.));
#8196=DIRECTION('',(0.,1.,0.));
#8197=DIRECTION('center_axis',(0.,-1.,0.));
#8198=DIRECTION('ref_axis',(1.,0.,0.));
#8199=DIRECTION('center_axis',(0.,1.,0.));
#8200=DIRECTION('ref_axis',(1.,0.,0.));
#8201=DIRECTION('center_axis',(0.,1.,0.));
#8202=DIRECTION('ref_axis',(1.,0.,0.));
#8203=DIRECTION('',(0.,1.,0.));
#8204=DIRECTION('center_axis',(0.,-1.,0.));
#8205=DIRECTION('ref_axis',(1.,0.,0.));
#8206=DIRECTION('center_axis',(0.,1.,0.));
#8207=DIRECTION('ref_axis',(1.,0.,0.));
#8208=DIRECTION('center_axis',(0.,1.,0.));
#8209=DIRECTION('ref_axis',(1.,0.,0.));
#8210=DIRECTION('',(0.,-1.,0.));
#8211=DIRECTION('center_axis',(0.,1.,0.));
#8212=DIRECTION('ref_axis',(1.,0.,0.));
#8213=DIRECTION('center_axis',(0.,1.,0.));
#8214=DIRECTION('ref_axis',(1.,0.,0.));
#8215=DIRECTION('center_axis',(0.,-1.,0.));
#8216=DIRECTION('ref_axis',(1.,0.,0.));
#8217=DIRECTION('center_axis',(0.,1.,0.));
#8218=DIRECTION('ref_axis',(1.,0.,0.));
#8219=DIRECTION('center_axis',(0.,-1.,0.));
#8220=DIRECTION('ref_axis',(1.,0.,0.));
#8221=DIRECTION('',(0.,-1.,0.));
#8222=DIRECTION('center_axis',(0.,1.,0.));
#8223=DIRECTION('ref_axis',(1.,0.,0.));
#8224=DIRECTION('center_axis',(0.,1.,0.));
#8225=DIRECTION('ref_axis',(1.,0.,0.));
#8226=DIRECTION('',(0.,-1.,0.));
#8227=DIRECTION('center_axis',(0.,1.,0.));
#8228=DIRECTION('ref_axis',(1.,0.,0.));
#8229=DIRECTION('center_axis',(0.,1.,0.));
#8230=DIRECTION('ref_axis',(1.,0.,0.));
#8231=DIRECTION('center_axis',(0.,1.,0.));
#8232=DIRECTION('ref_axis',(1.,0.,0.));
#10208=CARTESIAN_POINT('',(0.,0.,0.));
#10209=CARTESIAN_POINT('Origin',(-1.4142135623731,3.2,2.58578643762691));
#10210=CARTESIAN_POINT('',(-1.6392135623731,3.3,2.58578643762691));
#10211=CARTESIAN_POINT('Origin',(-1.4142135623731,3.3,2.58578643762691));
#10212=CARTESIAN_POINT('',(-1.6392135623731,3.5,2.58578643762691));
#10213=CARTESIAN_POINT('',(-1.6392135623731,3.2,2.58578643762691));
#10214=CARTESIAN_POINT('Origin',(-1.4142135623731,3.5,2.58578643762691));
#10215=CARTESIAN_POINT('Origin',(-1.41421356237309,3.2,5.41421356237309));
#10216=CARTESIAN_POINT('',(-1.6392135623731,3.3,5.41421356237309));
#10217=CARTESIAN_POINT('Origin',(-1.41421356237309,3.3,5.41421356237309));
#10218=CARTESIAN_POINT('',(-1.6392135623731,3.5,5.41421356237309));
#10219=CARTESIAN_POINT('',(-1.6392135623731,3.2,5.41421356237309));
#10220=CARTESIAN_POINT('Origin',(-1.41421356237309,3.5,5.41421356237309));
#10221=CARTESIAN_POINT('Origin',(1.4142135623731,3.2,5.41421356237309));
#10222=CARTESIAN_POINT('',(1.1892135623731,3.3,5.41421356237309));
#10223=CARTESIAN_POINT('Origin',(1.4142135623731,3.3,5.41421356237309));
#10224=CARTESIAN_POINT('',(1.1892135623731,3.5,5.41421356237309));
#10225=CARTESIAN_POINT('',(1.1892135623731,3.2,5.41421356237309));
#10226=CARTESIAN_POINT('Origin',(1.4142135623731,3.5,5.41421356237309));
#10227=CARTESIAN_POINT('Origin',(1.41421356237309,3.2,2.5857864376269));
#10228=CARTESIAN_POINT('',(1.18921356237309,3.3,2.5857864376269));
#10229=CARTESIAN_POINT('Origin',(1.41421356237309,3.3,2.5857864376269));
#10230=CARTESIAN_POINT('',(1.18921356237309,3.5,2.5857864376269));
#10231=CARTESIAN_POINT('',(1.18921356237309,3.2,2.5857864376269));
#10232=CARTESIAN_POINT('Origin',(1.41421356237309,3.5,2.5857864376269));
#10233=CARTESIAN_POINT('Origin',(0.,3.,4.));
#10234=CARTESIAN_POINT('',(-1.59,3.3,4.));
#10235=CARTESIAN_POINT('Origin',(0.,3.3,4.));
#10236=CARTESIAN_POINT('',(-1.59,3.,4.));
#10237=CARTESIAN_POINT('',(-1.59,3.,4.));
#10238=CARTESIAN_POINT('Origin',(0.,3.,4.));
#10239=CARTESIAN_POINT('Origin',(0.,3.,4.));
#10240=CARTESIAN_POINT('',(-1.005,3.,4.));
#10241=CARTESIAN_POINT('Origin',(0.,3.,4.));
#10242=CARTESIAN_POINT('Origin',(0.,3.3,4.));
#10243=CARTESIAN_POINT('',(-1.005,3.5,4.));
#10244=CARTESIAN_POINT('Origin',(0.,3.5,4.));
#10245=CARTESIAN_POINT('',(-1.005,3.3,4.));
#10246=CARTESIAN_POINT('Origin',(0.,3.3,4.));
#10247=CARTESIAN_POINT('',(-2.4,3.5,4.));
#10248=CARTESIAN_POINT('Origin',(0.,3.5,4.));
#10249=CARTESIAN_POINT('',(-2.4,3.3,4.));
#10250=CARTESIAN_POINT('',(-2.4,3.3,4.));
#10251=CARTESIAN_POINT('Origin',(0.,3.3,4.));
#10252=CARTESIAN_POINT('Origin',(0.,3.5,4.));
#10253=CARTESIAN_POINT('Origin',(0.,3.3,4.));
#13200=UNCERTAINTY_MEASURE_WITH_UNIT(LENGTH_MEASURE(0.001),#13278,
'DISTANCE_ACCURACY_VALUE',
'Maximum model space distance between geometric entities at asserted c
onnectivities');
#13233=UNCERTAINTY_MEASURE_WITH_UNIT(LENGTH_MEASURE(0.001),#13278,
'DISTANCE_ACCURACY_VALUE',
'Maximum model space distance between geometric entities at asserted c
onnectivities');
#13244=(
GEOMETRIC_REPRESENTATION_CONTEXT(3)
GLOBAL_UNCERTAINTY_ASSIGNED_CONTEXT((#13200))
GLOBAL_UNIT_ASSIGNED_CONTEXT((#13278,#13280,#13281))
REPRESENTATION_CONTEXT('','3D')
);
#13277=(
GEOMETRIC_REPRESENTATION_CONTEXT(3)
GLOBAL_UNCERTAINTY_ASSIGNED_CONTEXT((#13233))
GLOBAL_UNIT_ASSIGNED_CONTEXT((#13278,#13280,#13281))
REPRESENTATION_CONTEXT('','3D')
);
#13278=(
LENGTH_UNIT()
NAMED_UNIT(*)
SI_UNIT(.CENTI.,.METRE.)
);
#13280=(
NAMED_UNIT(*)
PLANE_ANGLE_UNIT()
SI_UNIT($,.RADIAN.)
);
#13281=(
NAMED_UNIT(*)
SI_UNIT($,.STERADIAN.)
SOLID_ANGLE_UNIT()
);
#13292=SHAPE_DEFINITION_REPRESENTATION(#13335,#13449);
#13335=PRODUCT_DEFINITION_SHAPE('',$,#13493);
#13449=SHAPE_REPRESENTATION('',(#7038),#13244);
#13482=PRODUCT_DEFINITION_CONTEXT('part definition',#13613,'design');
#13493=PRODUCT_DEFINITION('Bearing cap (3)','Bearing cap (3)',#13536,#13482);
#13536=PRODUCT_DEFINITION_FORMATION('',$,#13625);
#13613=APPLICATION_CONTEXT(
'Core Data for Automotive Mechanical Design Process');
#13614=PRODUCT_CONTEXT('part definition',#13613,'mechanical');
#13625=PRODUCT('Bearing cap (3)','Bearing cap (3)','Bearing cap (3)',(#13614));
#13714=COLOUR_RGB('Grey',0.48,0.52,0.57);
#13715=FILL_AREA_STYLE_COLOUR('',#13714);
#13716=FILL_AREA_STYLE('',(#13715));
#13717=SURFACE_STYLE_FILL_AREA(#13716);
#13718=SURFACE_SIDE_STYLE('',(#13717));
#13719=SURFACE_STYLE_USAGE(.BOTH.,#13718);
#13720=PRESENTATION_STYLE_ASSIGNMENT((#13719));
ENDSEC;
END-ISO-10303-21;
